ISO-10303-21;
HEADER;
/* Generated by software containing ST-Developer
 * from STEP Tools, Inc. (www.steptools.com) 
 */

FILE_DESCRIPTION(
/* description */ ('Union bypass pipe loop'),
/* implementation_level */ '2;1');

FILE_NAME(
/* name */ 'Hex Nut - M5.step',
/* time_stamp */ '2026-10-27T21:00:29-07:00',
/* author */ (''),
/* organization */ (''),
/* preprocessor_version */ 'ST-DEVELOPER v20.2',
/* originating_system */ 'Autodesk Translation Framework v15.17.0.0',
/* authorisation */ '');

FILE_SCHEMA (('AUTOMOTIVE_DESIGN { 1 0 10303 214 3 1 1 }'));
ENDSEC;

DATA;
#10=MECHANICAL_DESIGN_GEOMETRIC_PRESENTATION_REPRESENTATION('',(#455),#10095);
#327=(
BOUNDED_CURVE()
B_SPLINE_CURVE(2,(#8945,#8946,#8947),.UNSPECIFIED.,.F.,.F.)
B_SPLINE_CURVE_WITH_KNOTS((3,3),(0.140651836354967,0.670383167684795),
 .UNSPECIFIED.)
CURVE()
GEOMETRIC_REPRESENTATION_ITEM()
RATIONAL_B_SPLINE_CURVE((1.11602540378444,1.28867513459481,1.11602540378444))
REPRESENTATION_ITEM('')
);
#328=(
BOUNDED_CURVE()
B_SPLINE_CURVE(2,(#8949,#8950,#8951),.UNSPECIFIED.,.F.,.F.)
B_SPLINE_CURVE_WITH_KNOTS((3,3),(0.140651836354967,0.670383167684795),
 .UNSPECIFIED.)
CURVE()
GEOMETRIC_REPRESENTATION_ITEM()
RATIONAL_B_SPLINE_CURVE((1.11602540378444,1.28867513459481,1.11602540378444))
REPRESENTATION_ITEM('')
);
#329=(
BOUNDED_CURVE()
B_SPLINE_CURVE(2,(#8956,#8957,#8958),.UNSPECIFIED.,.F.,.F.)
B_SPLINE_CURVE_WITH_KNOTS((3,3),(0.140651836354967,0.670383167684795),
 .UNSPECIFIED.)
CURVE()
GEOMETRIC_REPRESENTATION_ITEM()
RATIONAL_B_SPLINE_CURVE((1.11602540378444,1.28867513459481,1.11602540378444))
REPRESENTATION_ITEM('')
);
#330=(
BOUNDED_CURVE()
B_SPLINE_CURVE(2,(#8960,#8961,#8962),.UNSPECIFIED.,.F.,.F.)
B_SPLINE_CURVE_WITH_KNOTS((3,3),(0.140651836354967,0.670383167684795),
 .UNSPECIFIED.)
CURVE()
GEOMETRIC_REPRESENTATION_ITEM()
RATIONAL_B_SPLINE_CURVE((1.11602540378444,1.28867513459481,1.11602540378444))
REPRESENTATION_ITEM('')
);
#331=(
BOUNDED_CURVE()
B_SPLINE_CURVE(2,(#8964,#8965,#8966),.UNSPECIFIED.,.F.,.F.)
B_SPLINE_CURVE_WITH_KNOTS((3,3),(0.140651836354967,0.670383167684795),
 .UNSPECIFIED.)
CURVE()
GEOMETRIC_REPRESENTATION_ITEM()
RATIONAL_B_SPLINE_CURVE((1.11602540378444,1.28867513459481,1.11602540378444))
REPRESENTATION_ITEM('')
);
#332=(
BOUNDED_CURVE()
B_SPLINE_CURVE(2,(#8967,#8968,#8969),.UNSPECIFIED.,.F.,.F.)
B_SPLINE_CURVE_WITH_KNOTS((3,3),(0.140651836354967,0.670383167684795),
 .UNSPECIFIED.)
CURVE()
GEOMETRIC_REPRESENTATION_ITEM()
RATIONAL_B_SPLINE_CURVE((1.11602540378444,1.28867513459481,1.11602540378444))
REPRESENTATION_ITEM('')
);
#333=(
BOUNDED_CURVE()
B_SPLINE_CURVE(2,(#8976,#8977,#8978),.UNSPECIFIED.,.F.,.F.)
B_SPLINE_CURVE_WITH_KNOTS((3,3),(0.140651836354967,0.670383167684795),
 .UNSPECIFIED.)
CURVE()
GEOMETRIC_REPRESENTATION_ITEM()
RATIONAL_B_SPLINE_CURVE((1.11602540378444,1.28867513459481,1.11602540378444))
REPRESENTATION_ITEM('')
);
#334=(
BOUNDED_CURVE()
B_SPLINE_CURVE(2,(#8980,#8981,#8982),.UNSPECIFIED.,.F.,.F.)
B_SPLINE_CURVE_WITH_KNOTS((3,3),(0.140651836354967,0.670383167684796),
 .UNSPECIFIED.)
CURVE()
GEOMETRIC_REPRESENTATION_ITEM()
RATIONAL_B_SPLINE_CURVE((1.11602540378444,1.28867513459481,1.11602540378444))
REPRESENTATION_ITEM('')
);
#335=(
BOUNDED_CURVE()
B_SPLINE_CURVE(2,(#8984,#8985,#8986),.UNSPECIFIED.,.F.,.F.)
B_SPLINE_CURVE_WITH_KNOTS((3,3),(0.140651836354967,0.670383167684795),
 .UNSPECIFIED.)
CURVE()
GEOMETRIC_REPRESENTATION_ITEM()
RATIONAL_B_SPLINE_CURVE((1.11602540378444,1.28867513459481,1.11602540378444))
REPRESENTATION_ITEM('')
);
#336=(
BOUNDED_CURVE()
B_SPLINE_CURVE(2,(#8988,#8989,#8990),.UNSPECIFIED.,.F.,.F.)
B_SPLINE_CURVE_WITH_KNOTS((3,3),(0.140651836354967,0.670383167684795),
 .UNSPECIFIED.)
CURVE()
GEOMETRIC_REPRESENTATION_ITEM()
RATIONAL_B_SPLINE_CURVE((1.11602540378444,1.28867513459482,1.11602540378444))
REPRESENTATION_ITEM('')
);
#337=(
BOUNDED_CURVE()
B_SPLINE_CURVE(2,(#8992,#8993,#8994),.UNSPECIFIED.,.F.,.F.)
B_SPLINE_CURVE_WITH_KNOTS((3,3),(0.140651836354967,0.670383167684795),
 .UNSPECIFIED.)
CURVE()
GEOMETRIC_REPRESENTATION_ITEM()
RATIONAL_B_SPLINE_CURVE((1.11602540378444,1.28867513459481,1.11602540378444))
REPRESENTATION_ITEM('')
);
#338=(
BOUNDED_CURVE()
B_SPLINE_CURVE(2,(#8995,#8996,#8997),.UNSPECIFIED.,.F.,.F.)
B_SPLINE_CURVE_WITH_KNOTS((3,3),(0.140651836354967,0.670383167684795),
 .UNSPECIFIED.)
CURVE()
GEOMETRIC_REPRESENTATION_ITEM()
RATIONAL_B_SPLINE_CURVE((1.11602540378444,1.28867513459481,1.11602540378444))
REPRESENTATION_ITEM('')
);
#355=CONICAL_SURFACE('',#6132,0.47094010767585,1.0471975511966);
#356=CONICAL_SURFACE('',#6134,0.47094010767585,1.0471975511966);
#391=SHAPE_REPRESENTATION_RELATIONSHIP('SRR','None',#10260,#423);
#423=ADVANCED_BREP_SHAPE_REPRESENTATION('',(#486),#10072);
#455=STYLED_ITEM('',(#10507),#486);
#486=MANIFOLD_SOLID_BREP('Body1',#5527);
#572=FACE_BOUND('',#1352,.T.);
#573=FACE_BOUND('',#1354,.T.);
#698=PLANE('',#6136);
#699=PLANE('',#6137);
#700=PLANE('',#6138);
#701=PLANE('',#6142);
#702=PLANE('',#6143);
#703=PLANE('',#6144);
#704=PLANE('',#6145);
#705=PLANE('',#6146);
#949=FACE_OUTER_BOUND('',#1342,.T.);
#950=FACE_OUTER_BOUND('',#1343,.T.);
#951=FACE_OUTER_BOUND('',#1344,.T.);
#952=FACE_OUTER_BOUND('',#1345,.T.);
#953=FACE_OUTER_BOUND('',#1346,.T.);
#954=FACE_OUTER_BOUND('',#1347,.T.);
#955=FACE_OUTER_BOUND('',#1348,.T.);
#956=FACE_OUTER_BOUND('',#1349,.T.);
#957=FACE_OUTER_BOUND('',#1350,.T.);
#958=FACE_OUTER_BOUND('',#1351,.T.);
#959=FACE_OUTER_BOUND('',#1353,.T.);
#1342=EDGE_LOOP('',(#4208,#4209,#4210,#4211,#4212,#4213,#4214,#4215,#4216));
#1343=EDGE_LOOP('',(#4217,#4218,#4219,#4220,#4221,#4222,#4223,#4224,#4225));
#1344=EDGE_LOOP('',(#4226,#4227,#4228,#4229));
#1345=EDGE_LOOP('',(#4230,#4231,#4232,#4233));
#1346=EDGE_LOOP('',(#4234,#4235,#4236,#4237));
#1347=EDGE_LOOP('',(#4238,#4239,#4240,#4241));
#1348=EDGE_LOOP('',(#4242,#4243,#4244,#4245));
#1349=EDGE_LOOP('',(#4246,#4247,#4248,#4249));
#1350=EDGE_LOOP('',(#4250,#4251,#4252,#4253));
#1351=EDGE_LOOP('',(#4254));
#1352=EDGE_LOOP('',(#4255));
#1353=EDGE_LOOP('',(#4256));
#1354=EDGE_LOOP('',(#4257));
#1759=LINE('',#8953,#2135);
#1760=LINE('',#8974,#2136);
#1761=LINE('',#8999,#2137);
#1762=LINE('',#9000,#2138);
#1763=LINE('',#9002,#2139);
#1764=LINE('',#9004,#2140);
#1765=LINE('',#9009,#2141);
#1766=LINE('',#9012,#2142);
#1767=LINE('',#9014,#2143);
#2135=VECTOR('',#7211,0.47094010767585);
#2136=VECTOR('',#7218,0.47094010767585);
#2137=VECTOR('',#7221,1.);
#2138=VECTOR('',#7222,1.);
#2139=VECTOR('',#7225,1.);
#2140=VECTOR('',#7228,1.);
#2141=VECTOR('',#7233,0.25);
#2142=VECTOR('',#7238,1.);
#2143=VECTOR('',#7241,1.);
#2474=CIRCLE('',#6133,0.38);
#2475=CIRCLE('',#6135,0.38);
#2476=CIRCLE('',#6140,0.2117);
#2477=CIRCLE('',#6141,0.2117);
#2786=VERTEX_POINT('',#8943);
#2787=VERTEX_POINT('',#8944);
#2788=VERTEX_POINT('',#8948);
#2789=VERTEX_POINT('',#8952);
#2790=VERTEX_POINT('',#8955);
#2791=VERTEX_POINT('',#8959);
#2792=VERTEX_POINT('',#8963);
#2793=VERTEX_POINT('',#8971);
#2794=VERTEX_POINT('',#8973);
#2795=VERTEX_POINT('',#8975);
#2796=VERTEX_POINT('',#8979);
#2797=VERTEX_POINT('',#8983);
#2798=VERTEX_POINT('',#8987);
#2799=VERTEX_POINT('',#8991);
#2800=VERTEX_POINT('',#9006);
#2801=VERTEX_POINT('',#9008);
#3302=EDGE_CURVE('',#2786,#2787,#327,.T.);
#3303=EDGE_CURVE('',#2788,#2786,#328,.T.);
#3304=EDGE_CURVE('',#2788,#2789,#1759,.T.);
#3305=EDGE_CURVE('',#2789,#2789,#2474,.T.);
#3306=EDGE_CURVE('',#2790,#2788,#329,.T.);
#3307=EDGE_CURVE('',#2791,#2790,#330,.T.);
#3308=EDGE_CURVE('',#2792,#2791,#331,.T.);
#3309=EDGE_CURVE('',#2787,#2792,#332,.T.);
#3310=EDGE_CURVE('',#2793,#2793,#2475,.T.);
#3311=EDGE_CURVE('',#2793,#2794,#1760,.T.);
#3312=EDGE_CURVE('',#2795,#2794,#333,.T.);
#3313=EDGE_CURVE('',#2796,#2795,#334,.T.);
#3314=EDGE_CURVE('',#2797,#2796,#335,.T.);
#3315=EDGE_CURVE('',#2798,#2797,#336,.T.);
#3316=EDGE_CURVE('',#2799,#2798,#337,.T.);
#3317=EDGE_CURVE('',#2794,#2799,#338,.T.);
#3318=EDGE_CURVE('',#2790,#2799,#1761,.T.);
#3319=EDGE_CURVE('',#2791,#2798,#1762,.T.);
#3320=EDGE_CURVE('',#2788,#2794,#1763,.T.);
#3321=EDGE_CURVE('',#2786,#2795,#1764,.T.);
#3322=EDGE_CURVE('',#2800,#2800,#2476,.F.);
#3323=EDGE_CURVE('',#2800,#2801,#1765,.T.);
#3324=EDGE_CURVE('',#2801,#2801,#2477,.F.);
#3325=EDGE_CURVE('',#2787,#2796,#1766,.T.);
#3326=EDGE_CURVE('',#2792,#2797,#1767,.T.);
#4208=ORIENTED_EDGE('',*,*,#3302,.F.);
#4209=ORIENTED_EDGE('',*,*,#3303,.F.);
#4210=ORIENTED_EDGE('',*,*,#3304,.T.);
#4211=ORIENTED_EDGE('',*,*,#3305,.F.);
#4212=ORIENTED_EDGE('',*,*,#3304,.F.);
#4213=ORIENTED_EDGE('',*,*,#3306,.F.);
#4214=ORIENTED_EDGE('',*,*,#3307,.F.);
#4215=ORIENTED_EDGE('',*,*,#3308,.F.);
#4216=ORIENTED_EDGE('',*,*,#3309,.F.);
#4217=ORIENTED_EDGE('',*,*,#3310,.F.);
#4218=ORIENTED_EDGE('',*,*,#3311,.T.);
#4219=ORIENTED_EDGE('',*,*,#3312,.F.);
#4220=ORIENTED_EDGE('',*,*,#3313,.F.);
#4221=ORIENTED_EDGE('',*,*,#3314,.F.);
#4222=ORIENTED_EDGE('',*,*,#3315,.F.);
#4223=ORIENTED_EDGE('',*,*,#3316,.F.);
#4224=ORIENTED_EDGE('',*,*,#3317,.F.);
#4225=ORIENTED_EDGE('',*,*,#3311,.F.);
#4226=ORIENTED_EDGE('',*,*,#3307,.T.);
#4227=ORIENTED_EDGE('',*,*,#3318,.T.);
#4228=ORIENTED_EDGE('',*,*,#3316,.T.);
#4229=ORIENTED_EDGE('',*,*,#3319,.F.);
#4230=ORIENTED_EDGE('',*,*,#3306,.T.);
#4231=ORIENTED_EDGE('',*,*,#3320,.T.);
#4232=ORIENTED_EDGE('',*,*,#3317,.T.);
#4233=ORIENTED_EDGE('',*,*,#3318,.F.);
#4234=ORIENTED_EDGE('',*,*,#3303,.T.);
#4235=ORIENTED_EDGE('',*,*,#3321,.T.);
#4236=ORIENTED_EDGE('',*,*,#3312,.T.);
#4237=ORIENTED_EDGE('',*,*,#3320,.F.);
#4238=ORIENTED_EDGE('',*,*,#3322,.F.);
#4239=ORIENTED_EDGE('',*,*,#3323,.T.);
#4240=ORIENTED_EDGE('',*,*,#3324,.T.);
#4241=ORIENTED_EDGE('',*,*,#3323,.F.);
#4242=ORIENTED_EDGE('',*,*,#3302,.T.);
#4243=ORIENTED_EDGE('',*,*,#3325,.T.);
#4244=ORIENTED_EDGE('',*,*,#3313,.T.);
#4245=ORIENTED_EDGE('',*,*,#3321,.F.);
#4246=ORIENTED_EDGE('',*,*,#3308,.T.);
#4247=ORIENTED_EDGE('',*,*,#3319,.T.);
#4248=ORIENTED_EDGE('',*,*,#3315,.T.);
#4249=ORIENTED_EDGE('',*,*,#3326,.F.);
#4250=ORIENTED_EDGE('',*,*,#3309,.T.);
#4251=ORIENTED_EDGE('',*,*,#3326,.T.);
#4252=ORIENTED_EDGE('',*,*,#3314,.T.);
#4253=ORIENTED_EDGE('',*,*,#3325,.F.);
#4254=ORIENTED_EDGE('',*,*,#3310,.T.);
#4255=ORIENTED_EDGE('',*,*,#3322,.T.);
#4256=ORIENTED_EDGE('',*,*,#3305,.T.);
#4257=ORIENTED_EDGE('',*,*,#3324,.F.);
#5123=CYLINDRICAL_SURFACE('',#6139,0.2117);
#5298=ADVANCED_FACE('',(#949),#355,.T.);
#5299=ADVANCED_FACE('',(#950),#356,.T.);
#5300=ADVANCED_FACE('',(#951),#698,.T.);
#5301=ADVANCED_FACE('',(#952),#699,.T.);
#5302=ADVANCED_FACE('',(#953),#700,.T.);
#5303=ADVANCED_FACE('',(#954),#5123,.F.);
#5304=ADVANCED_FACE('',(#955),#701,.T.);
#5305=ADVANCED_FACE('',(#956),#702,.T.);
#5306=ADVANCED_FACE('',(#957),#703,.T.);
#5307=ADVANCED_FACE('',(#958,#572),#704,.T.);
#5308=ADVANCED_FACE('',(#959,#573),#705,.F.);
#5527=CLOSED_SHELL('',(#5298,#5299,#5300,#5301,#5302,#5303,#5304,#5305,
#5306,#5307,#5308));
#6131=AXIS2_PLACEMENT_3D('',#8941,#7207,#7208);
#6132=AXIS2_PLACEMENT_3D('',#8942,#7209,#7210);
#6133=AXIS2_PLACEMENT_3D('',#8954,#7212,#7213);
#6134=AXIS2_PLACEMENT_3D('',#8970,#7214,#7215);
#6135=AXIS2_PLACEMENT_3D('',#8972,#7216,#7217);
#6136=AXIS2_PLACEMENT_3D('',#8998,#7219,#7220);
#6137=AXIS2_PLACEMENT_3D('',#9001,#7223,#7224);
#6138=AXIS2_PLACEMENT_3D('',#9003,#7226,#7227);
#6139=AXIS2_PLACEMENT_3D('',#9005,#7229,#7230);
#6140=AXIS2_PLACEMENT_3D('',#9007,#7231,#7232);
#6141=AXIS2_PLACEMENT_3D('',#9010,#7234,#7235);
#6142=AXIS2_PLACEMENT_3D('',#9011,#7236,#7237);
#6143=AXIS2_PLACEMENT_3D('',#9013,#7239,#7240);
#6144=AXIS2_PLACEMENT_3D('',#9015,#7242,#7243);
#6145=AXIS2_PLACEMENT_3D('',#9016,#7244,#7245);
#6146=AXIS2_PLACEMENT_3D('',#9017,#7246,#7247);
#7207=DIRECTION('axis',(0.,0.,1.));
#7208=DIRECTION('refdir',(1.,0.,0.));
#7209=DIRECTION('center_axis',(0.,1.,0.));
#7210=DIRECTION('ref_axis',(1.,0.,0.));
#7211=DIRECTION('',(0.866025403784439,-0.5,1.06057523872491E-16));
#7212=DIRECTION('center_axis',(0.,-1.,0.));
#7213=DIRECTION('ref_axis',(1.,0.,0.));
#7214=DIRECTION('center_axis',(0.,-1.,0.));
#7215=DIRECTION('ref_axis',(1.,0.,0.));
#7216=DIRECTION('center_axis',(0.,1.,0.));
#7217=DIRECTION('ref_axis',(1.,0.,0.));
#7218=DIRECTION('',(-0.866025403784439,-0.5,-1.06057523872491E-16));
#7219=DIRECTION('center_axis',(1.20185167898973E-16,0.,-1.));
#7220=DIRECTION('ref_axis',(-1.,0.,-1.20185167898973E-16));
#7221=DIRECTION('',(0.,1.,0.));
#7222=DIRECTION('',(0.,1.,0.));
#7223=DIRECTION('center_axis',(-0.866025403784439,0.,-0.5));
#7224=DIRECTION('ref_axis',(-0.5,0.,0.866025403784439));
#7225=DIRECTION('',(0.,1.,0.));
#7226=DIRECTION('center_axis',(-0.866025403784439,0.,0.5));
#7227=DIRECTION('ref_axis',(0.5,0.,0.866025403784439));
#7228=DIRECTION('',(0.,1.,0.));
#7229=DIRECTION('center_axis',(0.,1.,0.));
#7230=DIRECTION('ref_axis',(1.,0.,0.));
#7231=DIRECTION('center_axis',(0.,1.,0.));
#7232=DIRECTION('ref_axis',(1.,0.,0.));
#7233=DIRECTION('',(0.,-1.,0.));
#7234=DIRECTION('center_axis',(0.,1.,0.));
#7235=DIRECTION('ref_axis',(1.,0.,0.));
#7236=DIRECTION('center_axis',(-2.40370335797945E-16,0.,1.));
#7237=DIRECTION('ref_axis',(1.,0.,2.40370335797945E-16));
#7238=DIRECTION('',(0.,1.,0.));
#7239=DIRECTION('center_axis',(0.866025403784439,0.,-0.5));
#7240=DIRECTION('ref_axis',(-0.5,0.,-0.866025403784439));
#7241=DIRECTION('',(0.,1.,0.));
#7242=DIRECTION('center_axis',(0.866025403784439,0.,0.5));
#7243=DIRECTION('ref_axis',(0.5,0.,-0.866025403784439));
#7244=DIRECTION('center_axis',(0.,1.,0.));
#7245=DIRECTION('ref_axis',(1.,0.,0.));
#7246=DIRECTION('center_axis',(0.,1.,0.));
#7247=DIRECTION('ref_axis',(1.,0.,0.));
#8941=CARTESIAN_POINT('',(0.,0.,0.));
#8942=CARTESIAN_POINT('Origin',(0.,0.0525042956467857,0.));
#8943=CARTESIAN_POINT('',(-0.230940107675851,0.0472735643746089,0.4));
#8944=CARTESIAN_POINT('',(0.23094010767585,0.0472735643746089,0.4));
#8945=CARTESIAN_POINT('Ctrl Pts',(-0.230940107675851,0.0472735643746089,
0.4));
#8946=CARTESIAN_POINT('Ctrl Pts',(1.11022302462516E-16,-0.0193931022920578,
0.4));
#8947=CARTESIAN_POINT('Ctrl Pts',(0.23094010767585,0.0472735643746089,0.4));
#8948=CARTESIAN_POINT('',(-0.461880215351701,0.0472735643746089,-5.6564012731995E-17));
#8949=CARTESIAN_POINT('Ctrl Pts',(-0.461880215351701,0.0472735643746089,
-5.6564012731995E-17));
#8950=CARTESIAN_POINT('Ctrl Pts',(-0.346410161513776,-0.0193931022920579,
0.2));
#8951=CARTESIAN_POINT('Ctrl Pts',(-0.230940107675851,0.0472735643746089,
0.4));
#8952=CARTESIAN_POINT('',(-0.38,-2.08166817117217E-17,-4.65365783675994E-17));
#8953=CARTESIAN_POINT('',(-0.47094010767585,0.0525042956467857,-5.7673529545534E-17));
#8954=CARTESIAN_POINT('Origin',(0.,0.,0.));
#8955=CARTESIAN_POINT('',(-0.23094010767585,0.0472735643746089,-0.4));
#8956=CARTESIAN_POINT('Ctrl Pts',(-0.23094010767585,0.0472735643746089,
-0.4));
#8957=CARTESIAN_POINT('Ctrl Pts',(-0.346410161513775,-0.0193931022920578,
-0.2));
#8958=CARTESIAN_POINT('Ctrl Pts',(-0.461880215351701,0.0472735643746089,
-5.6564012731995E-17));
#8959=CARTESIAN_POINT('',(0.23094010767585,0.0472735643746089,-0.4));
#8960=CARTESIAN_POINT('Ctrl Pts',(0.23094010767585,0.0472735643746089,-0.4));
#8961=CARTESIAN_POINT('Ctrl Pts',(0.,-0.0193931022920578,-0.4));
#8962=CARTESIAN_POINT('Ctrl Pts',(-0.23094010767585,0.0472735643746089,
-0.4));
#8963=CARTESIAN_POINT('',(0.461880215351701,0.0472735643746089,0.));
#8964=CARTESIAN_POINT('Ctrl Pts',(0.461880215351701,0.0472735643746089,
0.));
#8965=CARTESIAN_POINT('Ctrl Pts',(0.346410161513776,-0.019393102292058,
-0.2));
#8966=CARTESIAN_POINT('Ctrl Pts',(0.23094010767585,0.0472735643746089,-0.4));
#8967=CARTESIAN_POINT('Ctrl Pts',(0.23094010767585,0.0472735643746089,0.4));
#8968=CARTESIAN_POINT('Ctrl Pts',(0.346410161513776,-0.0193931022920577,
0.2));
#8969=CARTESIAN_POINT('Ctrl Pts',(0.461880215351701,0.0472735643746089,
0.));
#8970=CARTESIAN_POINT('Origin',(0.,0.417495704353214,0.));
#8971=CARTESIAN_POINT('',(-0.38,0.47,-4.65365783675994E-17));
#8972=CARTESIAN_POINT('Origin',(0.,0.47,0.));
#8973=CARTESIAN_POINT('',(-0.461880215351701,0.422726435625391,-5.6564012731995E-17));
#8974=CARTESIAN_POINT('',(-0.47094010767585,0.417495704353214,-5.7673529545534E-17));
#8975=CARTESIAN_POINT('',(-0.230940107675851,0.422726435625391,0.4));
#8976=CARTESIAN_POINT('Ctrl Pts',(-0.230940107675851,0.422726435625391,
0.4));
#8977=CARTESIAN_POINT('Ctrl Pts',(-0.346410161513776,0.489393102292058,
0.2));
#8978=CARTESIAN_POINT('Ctrl Pts',(-0.461880215351701,0.422726435625391,
-5.6564012731995E-17));
#8979=CARTESIAN_POINT('',(0.23094010767585,0.422726435625391,0.4));
#8980=CARTESIAN_POINT('Ctrl Pts',(0.23094010767585,0.422726435625391,0.4));
#8981=CARTESIAN_POINT('Ctrl Pts',(8.32667268468867E-17,0.489393102292058,
0.4));
#8982=CARTESIAN_POINT('Ctrl Pts',(-0.230940107675851,0.422726435625391,
0.4));
#8983=CARTESIAN_POINT('',(0.461880215351701,0.422726435625391,0.));
#8984=CARTESIAN_POINT('Ctrl Pts',(0.461880215351701,0.422726435625391,0.));
#8985=CARTESIAN_POINT('Ctrl Pts',(0.346410161513776,0.489393102292058,0.2));
#8986=CARTESIAN_POINT('Ctrl Pts',(0.23094010767585,0.422726435625391,0.4));
#8987=CARTESIAN_POINT('',(0.23094010767585,0.422726435625391,-0.4));
#8988=CARTESIAN_POINT('Ctrl Pts',(0.23094010767585,0.422726435625391,-0.4));
#8989=CARTESIAN_POINT('Ctrl Pts',(0.346410161513775,0.489393102292058,-0.2));
#8990=CARTESIAN_POINT('Ctrl Pts',(0.461880215351701,0.422726435625391,0.));
#8991=CARTESIAN_POINT('',(-0.23094010767585,0.422726435625391,-0.4));
#8992=CARTESIAN_POINT('Ctrl Pts',(-0.23094010767585,0.422726435625391,-0.4));
#8993=CARTESIAN_POINT('Ctrl Pts',(-5.55111512312578E-17,0.489393102292058,
-0.4));
#8994=CARTESIAN_POINT('Ctrl Pts',(0.23094010767585,0.422726435625391,-0.4));
#8995=CARTESIAN_POINT('Ctrl Pts',(-0.461880215351701,0.422726435625391,
-5.6564012731995E-17));
#8996=CARTESIAN_POINT('Ctrl Pts',(-0.346410161513776,0.489393102292058,
-0.2));
#8997=CARTESIAN_POINT('Ctrl Pts',(-0.23094010767585,0.422726435625391,-0.4));
#8998=CARTESIAN_POINT('Origin',(0.23094010767585,0.,-0.4));
#8999=CARTESIAN_POINT('',(-0.23094010767585,0.,-0.4));
#9000=CARTESIAN_POINT('',(0.23094010767585,0.,-0.4));
#9001=CARTESIAN_POINT('Origin',(-0.23094010767585,0.,-0.4));
#9002=CARTESIAN_POINT('',(-0.461880215351701,0.,-5.6564012731995E-17));
#9003=CARTESIAN_POINT('Origin',(-0.461880215351701,0.,-5.6564012731995E-17));
#9004=CARTESIAN_POINT('',(-0.230940107675851,0.,0.4));
#9005=CARTESIAN_POINT('Origin',(0.,0.,0.));
#9006=CARTESIAN_POINT('',(-0.2117,0.47,2.59257727379495E-17));
#9007=CARTESIAN_POINT('Origin',(0.,0.47,0.));
#9008=CARTESIAN_POINT('',(-0.2117,0.,2.59257727379495E-17));
#9009=CARTESIAN_POINT('',(-0.2117,0.,2.59257727379495E-17));
#9010=CARTESIAN_POINT('Origin',(0.,0.,0.));
#9011=CARTESIAN_POINT('Origin',(-0.230940107675851,0.,0.4));
#9012=CARTESIAN_POINT('',(0.23094010767585,0.,0.4));
#9013=CARTESIAN_POINT('Origin',(0.461880215351701,0.,0.));
#9014=CARTESIAN_POINT('',(0.461880215351701,0.,0.));
#9015=CARTESIAN_POINT('Origin',(0.23094010767585,0.,0.4));
#9016=CARTESIAN_POINT('Origin',(0.,0.47,0.));
#9017=CARTESIAN_POINT('Origin',(0.,0.,0.));
#10035=UNCERTAINTY_MEASURE_WITH_UNIT(LENGTH_MEASURE(0.001),#10096,
'DISTANCE_ACCURACY_VALUE',
'Maximum model space distance between geometric entities at asserted c
onnectivities');
#10058=UNCERTAINTY_MEASURE_WITH_UNIT(LENGTH_MEASURE(0.001),#10096,
'DISTANCE_ACCURACY_VALUE',
'Maximum model space distance between geometric entities at asserted c
onnectivities');
#10072=(
GEOMETRIC_REPRESENTATION_CONTEXT(3)
GLOBAL_UNCERTAINTY_ASSIGNED_CONTEXT((#10035))
GLOBAL_UNIT_ASSIGNED_CONTEXT((#10096,#10098,#10099))
REPRESENTATION_CONTEXT('','3D')
);
#10095=(
GEOMETRIC_REPRESENTATION_CONTEXT(3)
GLOBAL_UNCERTAINTY_ASSIGNED_CONTEXT((#10058))
GLOBAL_UNIT_ASSIGNED_CONTEXT((#10096,#10098,#10099))
REPRESENTATION_CONTEXT('','3D')
);
#10096=(
LENGTH_UNIT()
NAMED_UNIT(*)
SI_UNIT(.CENTI.,.METRE.)
);
#10098=(
NAMED_UNIT(*)
PLANE_ANGLE_UNIT()
SI_UNIT($,.RADIAN.)
);
#10099=(
NAMED_UNIT(*)
SI_UNIT($,.STERADIAN.)
SOLID_ANGLE_UNIT()
);
#10113=SHAPE_DEFINITION_REPRESENTATION(#10149,#10260);
#10149=PRODUCT_DEFINITION_SHAPE('',$,#10297);
#10260=SHAPE_REPRESENTATION('',(#6131),#10072);
#10283=PRODUCT_DEFINITION_CONTEXT('part definition',#10393,'design');
#10297=PRODUCT_DEFINITION('Hex Nut - M5','Hex Nut - M5',#10333,#10283);
#10333=PRODUCT_DEFINITION_FORMATION('',$,#10408);
#10393=APPLICATION_CONTEXT(
'Core Data for Automotive Mechanical Design Process');
#10394=PRODUCT_CONTEXT('part definition',#10393,'mechanical');
#10408=PRODUCT('Hex Nut - M5','Hex Nut - M5','Hex Nut - M5',(#10394));
#10501=COLOUR_RGB('Black',0.12,0.14,0.17);
#10502=FILL_AREA_STYLE_COLOUR('',#10501);
#10503=FILL_AREA_STYLE('',(#10502));
#10504=SURFACE_STYLE_FILL_AREA(#10503);
#10505=SURFACE_SIDE_STYLE('',(#10504));
#10506=SURFACE_STYLE_USAGE(.BOTH.,#10505);
#10507=PRESENTATION_STYLE_ASSIGNMENT((#10506));
ENDSEC;
END-ISO-10303-21;
